ISO-10303-21;
HEADER;
/* Generated by software containing ST-Developer
 * from STEP Tools, Inc. (www.steptools.com) 
 */

FILE_DESCRIPTION(
/* description */ ('Independent equipment support assembly with bolted 600 x 500 mm welde
d perimeter frame, four adjustable legs and swivel feet. Nominal overa
ll height 518 mm. No load rating assigned.'),
/* implementation_level */ '2;1');

FILE_NAME(
/* name */ 'Flat washer M6.step',
/* time_stamp */ '2026-11-07T17:30:39-08:00',
/* author */ (''),
/* organization */ (''),
/* preprocessor_version */ 'ST-DEVELOPER v20.2',
/* originating_system */ 'Autodesk Translation Framework v15.17.0.0',
/* authorisation */ '');

FILE_SCHEMA (('AUTOMOTIVE_DESIGN { 1 0 10303 214 3 1 1 }'));
ENDSEC;

DATA;
#10=MECHANICAL_DESIGN_GEOMETRIC_PRESENTATION_REPRESENTATION('',(#2223),#63755);
#483=CIRCLE('',#15488,3.5);
#484=CIRCLE('',#15489,3.5);
#485=CIRCLE('',#15491,7.);
#486=CIRCLE('',#15492,7.);
#2174=CYLINDRICAL_SURFACE('',#15487,3.5);
#2175=CYLINDRICAL_SURFACE('',#15490,7.);
#2191=SHAPE_REPRESENTATION_RELATIONSHIP('SRR','None',#63876,#2207);
#2207=ADVANCED_BREP_SHAPE_REPRESENTATION('',(#2239),#63754);
#2223=STYLED_ITEM('',(#63961),#2239);
#2239=MANIFOLD_SOLID_BREP('Body1',#14324);
#2301=FACE_BOUND('',#3883,.T.);
#2302=FACE_BOUND('',#3885,.T.);
#3059=FACE_OUTER_BOUND('',#3880,.T.);
#3060=FACE_OUTER_BOUND('',#3881,.T.);
#3061=FACE_OUTER_BOUND('',#3882,.T.);
#3062=FACE_OUTER_BOUND('',#3884,.T.);
#3880=EDGE_LOOP('',(#13397,#13398,#13399,#13400));
#3881=EDGE_LOOP('',(#13401,#13402,#13403,#13404));
#3882=EDGE_LOOP('',(#13405));
#3883=EDGE_LOOP('',(#13406));
#3884=EDGE_LOOP('',(#13407));
#3885=EDGE_LOOP('',(#13408));
#4720=LINE('',#63686,#5556);
#4721=LINE('',#63692,#5557);
#5556=VECTOR('',#18323,3.5);
#5557=VECTOR('',#18330,7.);
#6982=VERTEX_POINT('',#63683);
#6983=VERTEX_POINT('',#63685);
#6984=VERTEX_POINT('',#63689);
#6985=VERTEX_POINT('',#63691);
#9121=EDGE_CURVE('',#6982,#6982,#483,.T.);
#9122=EDGE_CURVE('',#6982,#6983,#4720,.T.);
#9123=EDGE_CURVE('',#6983,#6983,#484,.T.);
#9124=EDGE_CURVE('',#6984,#6984,#485,.T.);
#9125=EDGE_CURVE('',#6984,#6985,#4721,.T.);
#9126=EDGE_CURVE('',#6985,#6985,#486,.T.);
#13397=ORIENTED_EDGE('',*,*,#9121,.F.);
#13398=ORIENTED_EDGE('',*,*,#9122,.T.);
#13399=ORIENTED_EDGE('',*,*,#9123,.T.);
#13400=ORIENTED_EDGE('',*,*,#9122,.F.);
#13401=ORIENTED_EDGE('',*,*,#9124,.F.);
#13402=ORIENTED_EDGE('',*,*,#9125,.T.);
#13403=ORIENTED_EDGE('',*,*,#9126,.T.);
#13404=ORIENTED_EDGE('',*,*,#9125,.F.);
#13405=ORIENTED_EDGE('',*,*,#9124,.T.);
#13406=ORIENTED_EDGE('',*,*,#9121,.T.);
#13407=ORIENTED_EDGE('',*,*,#9126,.F.);
#13408=ORIENTED_EDGE('',*,*,#9123,.F.);
#13547=PLANE('',#15493);
#13548=PLANE('',#15494);
#14305=ADVANCED_FACE('',(#3059),#2174,.F.);
#14306=ADVANCED_FACE('',(#3060),#2175,.T.);
#14307=ADVANCED_FACE('',(#3061,#2301),#13547,.T.);
#14308=ADVANCED_FACE('',(#3062,#2302),#13548,.F.);
#14324=CLOSED_SHELL('',(#14305,#14306,#14307,#14308));
#15486=AXIS2_PLACEMENT_3D('',#63681,#18317,#18318);
#15487=AXIS2_PLACEMENT_3D('',#63682,#18319,#18320);
#15488=AXIS2_PLACEMENT_3D('',#63684,#18321,#18322);
#15489=AXIS2_PLACEMENT_3D('',#63687,#18324,#18325);
#15490=AXIS2_PLACEMENT_3D('',#63688,#18326,#18327);
#15491=AXIS2_PLACEMENT_3D('',#63690,#18328,#18329);
#15492=AXIS2_PLACEMENT_3D('',#63693,#18331,#18332);
#15493=AXIS2_PLACEMENT_3D('',#63694,#18333,#18334);
#15494=AXIS2_PLACEMENT_3D('',#63695,#18335,#18336);
#18317=DIRECTION('axis',(0.,0.,1.));
#18318=DIRECTION('refdir',(1.,0.,0.));
#18319=DIRECTION('center_axis',(0.,0.,1.));
#18320=DIRECTION('ref_axis',(1.,0.,0.));
#18321=DIRECTION('center_axis',(0.,0.,-1.));
#18322=DIRECTION('ref_axis',(1.,0.,0.));
#18323=DIRECTION('',(0.,0.,-1.));
#18324=DIRECTION('center_axis',(0.,0.,-1.));
#18325=DIRECTION('ref_axis',(1.,0.,0.));
#18326=DIRECTION('center_axis',(0.,0.,1.));
#18327=DIRECTION('ref_axis',(1.,0.,0.));
#18328=DIRECTION('center_axis',(0.,0.,1.));
#18329=DIRECTION('ref_axis',(1.,0.,0.));
#18330=DIRECTION('',(0.,0.,-1.));
#18331=DIRECTION('center_axis',(0.,0.,1.));
#18332=DIRECTION('ref_axis',(1.,0.,0.));
#18333=DIRECTION('center_axis',(0.,0.,1.));
#18334=DIRECTION('ref_axis',(1.,0.,0.));
#18335=DIRECTION('center_axis',(0.,0.,1.));
#18336=DIRECTION('ref_axis',(1.,0.,0.));
#63681=CARTESIAN_POINT('',(0.,0.,0.));
#63682=CARTESIAN_POINT('Origin',(0.,0.,0.));
#63683=CARTESIAN_POINT('',(-3.5,-4.28626379701574E-16,2.));
#63684=CARTESIAN_POINT('Origin',(0.,0.,2.));
#63685=CARTESIAN_POINT('',(-3.5,-4.28626379701574E-16,0.));
#63686=CARTESIAN_POINT('',(-3.5,-4.28626379701574E-16,0.));
#63687=CARTESIAN_POINT('Origin',(0.,0.,0.));
#63688=CARTESIAN_POINT('Origin',(0.,0.,0.));
#63689=CARTESIAN_POINT('',(-7.,-8.57252759403147E-16,2.));
#63690=CARTESIAN_POINT('Origin',(0.,0.,2.));
#63691=CARTESIAN_POINT('',(-7.,-8.57252759403147E-16,0.));
#63692=CARTESIAN_POINT('',(-7.,-8.57252759403147E-16,0.));
#63693=CARTESIAN_POINT('Origin',(0.,0.,0.));
#63694=CARTESIAN_POINT('Origin',(0.,0.,2.));
#63695=CARTESIAN_POINT('Origin',(0.,0.,0.));
#63734=UNCERTAINTY_MEASURE_WITH_UNIT(LENGTH_MEASURE(0.01),#63756,
'DISTANCE_ACCURACY_VALUE',
'Maximum model space distance between geometric entities at asserted c
onnectivities');
#63735=UNCERTAINTY_MEASURE_WITH_UNIT(LENGTH_MEASURE(0.01),#63756,
'DISTANCE_ACCURACY_VALUE',
'Maximum model space distance between geometric entities at asserted c
onnectivities');
#63754=(
GEOMETRIC_REPRESENTATION_CONTEXT(3)
GLOBAL_UNCERTAINTY_ASSIGNED_CONTEXT((#63734))
GLOBAL_UNIT_ASSIGNED_CONTEXT((#63756,#63758,#63759))
REPRESENTATION_CONTEXT('','3D')
);
#63755=(
GEOMETRIC_REPRESENTATION_CONTEXT(3)
GLOBAL_UNCERTAINTY_ASSIGNED_CONTEXT((#63735))
GLOBAL_UNIT_ASSIGNED_CONTEXT((#63756,#63758,#63759))
REPRESENTATION_CONTEXT('','3D')
);
#63756=(
LENGTH_UNIT()
NAMED_UNIT(*)
SI_UNIT(.MILLI.,.METRE.)
);
#63758=(
NAMED_UNIT(*)
PLANE_ANGLE_UNIT()
SI_UNIT($,.RADIAN.)
);
#63759=(
NAMED_UNIT(*)
SI_UNIT($,.STERADIAN.)
SOLID_ANGLE_UNIT()
);
#63778=SHAPE_DEFINITION_REPRESENTATION(#63837,#63876);
#63837=PRODUCT_DEFINITION_SHAPE('',$,#63896);
#63876=SHAPE_REPRESENTATION('',(#15486),#63754);
#63877=PRODUCT_DEFINITION_CONTEXT('part definition',#63936,'design');
#63896=PRODUCT_DEFINITION('Flat washer M6','Flat washer M6',#63915,#63877);
#63915=PRODUCT_DEFINITION_FORMATION('',$,#63956);
#63936=APPLICATION_CONTEXT(
'Core Data for Automotive Mechanical Design Process');
#63937=PRODUCT_CONTEXT('part definition',#63936,'mechanical');
#63956=PRODUCT('Flat washer M6','Flat washer M6',$,(#63937));
#63961=PRESENTATION_STYLE_ASSIGNMENT((#63968));
#63968=SURFACE_STYLE_USAGE(.BOTH.,#63975);
#63975=SURFACE_SIDE_STYLE('',(#63982));
#63982=SURFACE_STYLE_FILL_AREA(#63989);
#63989=FILL_AREA_STYLE('Light gray',(#63996));
#63996=FILL_AREA_STYLE_COLOUR('Light gray',#64003);
#64003=COLOUR_RGB('Light gray',0.725490196078431,0.752941176470588,0.792156862745098);
ENDSEC;
END-ISO-10303-21;
